ISO-10303-21;
HEADER;
/* Generated by software containing ST-Developer
 * from STEP Tools, Inc. (www.steptools.com) 
 */

FILE_DESCRIPTION(
/* description */ ('Cam-and-follower valve demonstrator'),
/* implementation_level */ '2;1');

FILE_NAME(
/* name */ 'Foot (1).step',
/* time_stamp */ '2026-10-28T03:25:17-07:00',
/* author */ (''),
/* organization */ (''),
/* preprocessor_version */ 'ST-DEVELOPER v20.2',
/* originating_system */ 'Autodesk Translation Framework v15.17.0.0',
/* authorisation */ '');

FILE_SCHEMA (('AUTOMOTIVE_DESIGN { 1 0 10303 214 3 1 1 }'));
ENDSEC;

DATA;
#10=MECHANICAL_DESIGN_GEOMETRIC_PRESENTATION_REPRESENTATION('',(#414),#12896);
#342=SHAPE_REPRESENTATION_RELATIONSHIP('SRR','None',#13058,#378);
#378=ADVANCED_BREP_SHAPE_REPRESENTATION('',(#457),#12858);
#414=STYLED_ITEM('',(#13344),#457);
#457=MANIFOLD_SOLID_BREP('Body1',#6181);
#1118=FACE_OUTER_BOUND('',#1499,.T.);
#1119=FACE_OUTER_BOUND('',#1500,.T.);
#1120=FACE_OUTER_BOUND('',#1501,.T.);
#1121=FACE_OUTER_BOUND('',#1502,.T.);
#1122=FACE_OUTER_BOUND('',#1503,.T.);
#1123=FACE_OUTER_BOUND('',#1504,.T.);
#1499=EDGE_LOOP('',(#4203,#4204,#4205,#4206));
#1500=EDGE_LOOP('',(#4207,#4208,#4209,#4210));
#1501=EDGE_LOOP('',(#4211,#4212,#4213,#4214));
#1502=EDGE_LOOP('',(#4215,#4216,#4217,#4218));
#1503=EDGE_LOOP('',(#4219,#4220,#4221,#4222));
#1504=EDGE_LOOP('',(#4223,#4224,#4225,#4226));
#2037=LINE('',#9541,#2459);
#2038=LINE('',#9543,#2460);
#2039=LINE('',#9545,#2461);
#2040=LINE('',#9546,#2462);
#2041=LINE('',#9549,#2463);
#2042=LINE('',#9551,#2464);
#2043=LINE('',#9552,#2465);
#2044=LINE('',#9555,#2466);
#2045=LINE('',#9557,#2467);
#2046=LINE('',#9558,#2468);
#2047=LINE('',#9560,#2469);
#2048=LINE('',#9561,#2470);
#2459=VECTOR('',#7538,1.);
#2460=VECTOR('',#7539,1.);
#2461=VECTOR('',#7540,1.);
#2462=VECTOR('',#7541,1.);
#2463=VECTOR('',#7544,1.);
#2464=VECTOR('',#7545,1.);
#2465=VECTOR('',#7546,1.);
#2466=VECTOR('',#7549,1.);
#2467=VECTOR('',#7550,1.);
#2468=VECTOR('',#7551,1.);
#2469=VECTOR('',#7554,1.);
#2470=VECTOR('',#7555,1.);
#2875=VERTEX_POINT('',#9539);
#2876=VERTEX_POINT('',#9540);
#2877=VERTEX_POINT('',#9542);
#2878=VERTEX_POINT('',#9544);
#2879=VERTEX_POINT('',#9548);
#2880=VERTEX_POINT('',#9550);
#2881=VERTEX_POINT('',#9554);
#2882=VERTEX_POINT('',#9556);
#3398=EDGE_CURVE('',#2875,#2876,#2037,.T.);
#3399=EDGE_CURVE('',#2876,#2877,#2038,.T.);
#3400=EDGE_CURVE('',#2878,#2877,#2039,.T.);
#3401=EDGE_CURVE('',#2875,#2878,#2040,.T.);
#3402=EDGE_CURVE('',#2879,#2875,#2041,.T.);
#3403=EDGE_CURVE('',#2880,#2878,#2042,.T.);
#3404=EDGE_CURVE('',#2879,#2880,#2043,.T.);
#3405=EDGE_CURVE('',#2881,#2879,#2044,.T.);
#3406=EDGE_CURVE('',#2882,#2880,#2045,.T.);
#3407=EDGE_CURVE('',#2881,#2882,#2046,.T.);
#3408=EDGE_CURVE('',#2876,#2881,#2047,.T.);
#3409=EDGE_CURVE('',#2877,#2882,#2048,.T.);
#4203=ORIENTED_EDGE('',*,*,#3398,.T.);
#4204=ORIENTED_EDGE('',*,*,#3399,.T.);
#4205=ORIENTED_EDGE('',*,*,#3400,.F.);
#4206=ORIENTED_EDGE('',*,*,#3401,.F.);
#4207=ORIENTED_EDGE('',*,*,#3402,.T.);
#4208=ORIENTED_EDGE('',*,*,#3401,.T.);
#4209=ORIENTED_EDGE('',*,*,#3403,.F.);
#4210=ORIENTED_EDGE('',*,*,#3404,.F.);
#4211=ORIENTED_EDGE('',*,*,#3405,.T.);
#4212=ORIENTED_EDGE('',*,*,#3404,.T.);
#4213=ORIENTED_EDGE('',*,*,#3406,.F.);
#4214=ORIENTED_EDGE('',*,*,#3407,.F.);
#4215=ORIENTED_EDGE('',*,*,#3408,.T.);
#4216=ORIENTED_EDGE('',*,*,#3407,.T.);
#4217=ORIENTED_EDGE('',*,*,#3409,.F.);
#4218=ORIENTED_EDGE('',*,*,#3399,.F.);
#4219=ORIENTED_EDGE('',*,*,#3409,.T.);
#4220=ORIENTED_EDGE('',*,*,#3406,.T.);
#4221=ORIENTED_EDGE('',*,*,#3403,.T.);
#4222=ORIENTED_EDGE('',*,*,#3400,.T.);
#4223=ORIENTED_EDGE('',*,*,#3408,.F.);
#4224=ORIENTED_EDGE('',*,*,#3398,.F.);
#4225=ORIENTED_EDGE('',*,*,#3402,.F.);
#4226=ORIENTED_EDGE('',*,*,#3405,.F.);
#5614=PLANE('',#6662);
#5615=PLANE('',#6663);
#5616=PLANE('',#6664);
#5617=PLANE('',#6665);
#5618=PLANE('',#6666);
#5619=PLANE('',#6667);
#5834=ADVANCED_FACE('',(#1118),#5614,.T.);
#5835=ADVANCED_FACE('',(#1119),#5615,.T.);
#5836=ADVANCED_FACE('',(#1120),#5616,.T.);
#5837=ADVANCED_FACE('',(#1121),#5617,.T.);
#5838=ADVANCED_FACE('',(#1122),#5618,.T.);
#5839=ADVANCED_FACE('',(#1123),#5619,.F.);
#6181=CLOSED_SHELL('',(#5834,#5835,#5836,#5837,#5838,#5839));
#6661=AXIS2_PLACEMENT_3D('',#9537,#7534,#7535);
#6662=AXIS2_PLACEMENT_3D('',#9538,#7536,#7537);
#6663=AXIS2_PLACEMENT_3D('',#9547,#7542,#7543);
#6664=AXIS2_PLACEMENT_3D('',#9553,#7547,#7548);
#6665=AXIS2_PLACEMENT_3D('',#9559,#7552,#7553);
#6666=AXIS2_PLACEMENT_3D('',#9562,#7556,#7557);
#6667=AXIS2_PLACEMENT_3D('',#9563,#7558,#7559);
#7534=DIRECTION('axis',(0.,0.,1.));
#7535=DIRECTION('refdir',(1.,0.,0.));
#7536=DIRECTION('center_axis',(0.,1.,0.));
#7537=DIRECTION('ref_axis',(-1.,0.,0.));
#7538=DIRECTION('',(-1.,0.,0.));
#7539=DIRECTION('',(0.,0.,1.));
#7540=DIRECTION('',(-1.,0.,0.));
#7541=DIRECTION('',(0.,0.,1.));
#7542=DIRECTION('center_axis',(1.,0.,0.));
#7543=DIRECTION('ref_axis',(0.,1.,0.));
#7544=DIRECTION('',(0.,1.,0.));
#7545=DIRECTION('',(0.,1.,0.));
#7546=DIRECTION('',(0.,0.,1.));
#7547=DIRECTION('center_axis',(0.,-1.,0.));
#7548=DIRECTION('ref_axis',(1.,0.,0.));
#7549=DIRECTION('',(1.,0.,0.));
#7550=DIRECTION('',(1.,0.,0.));
#7551=DIRECTION('',(0.,0.,1.));
#7552=DIRECTION('center_axis',(-1.,0.,0.));
#7553=DIRECTION('ref_axis',(0.,-1.,0.));
#7554=DIRECTION('',(0.,-1.,0.));
#7555=DIRECTION('',(0.,-1.,0.));
#7556=DIRECTION('center_axis',(0.,0.,1.));
#7557=DIRECTION('ref_axis',(1.,0.,0.));
#7558=DIRECTION('center_axis',(0.,0.,1.));
#7559=DIRECTION('ref_axis',(1.,0.,0.));
#9537=CARTESIAN_POINT('',(0.,0.,0.));
#9538=CARTESIAN_POINT('Origin',(6.,9.,-0.8));
#9539=CARTESIAN_POINT('',(6.,9.,-0.8));
#9540=CARTESIAN_POINT('',(5.,9.,-0.8));
#9541=CARTESIAN_POINT('',(6.,9.,-0.8));
#9542=CARTESIAN_POINT('',(5.,9.,0.));
#9543=CARTESIAN_POINT('',(5.,9.,-0.8));
#9544=CARTESIAN_POINT('',(6.,9.,0.));
#9545=CARTESIAN_POINT('',(6.,9.,0.));
#9546=CARTESIAN_POINT('',(6.,9.,-0.8));
#9547=CARTESIAN_POINT('Origin',(6.,-5.5,-0.8));
#9548=CARTESIAN_POINT('',(6.,-5.5,-0.8));
#9549=CARTESIAN_POINT('',(6.,-5.5,-0.8));
#9550=CARTESIAN_POINT('',(6.,-5.5,0.));
#9551=CARTESIAN_POINT('',(6.,-5.5,0.));
#9552=CARTESIAN_POINT('',(6.,-5.5,-0.8));
#9553=CARTESIAN_POINT('Origin',(5.,-5.5,-0.8));
#9554=CARTESIAN_POINT('',(5.,-5.5,-0.8));
#9555=CARTESIAN_POINT('',(5.,-5.5,-0.8));
#9556=CARTESIAN_POINT('',(5.,-5.5,0.));
#9557=CARTESIAN_POINT('',(5.,-5.5,0.));
#9558=CARTESIAN_POINT('',(5.,-5.5,-0.8));
#9559=CARTESIAN_POINT('Origin',(5.,9.,-0.8));
#9560=CARTESIAN_POINT('',(5.,9.,-0.8));
#9561=CARTESIAN_POINT('',(5.,9.,0.));
#9562=CARTESIAN_POINT('Origin',(5.5,1.75,0.));
#9563=CARTESIAN_POINT('Origin',(5.5,1.75,-0.8));
#12815=UNCERTAINTY_MEASURE_WITH_UNIT(LENGTH_MEASURE(0.001),#12897,
'DISTANCE_ACCURACY_VALUE',
'Maximum model space distance between geometric entities at asserted c
onnectivities');
#12853=UNCERTAINTY_MEASURE_WITH_UNIT(LENGTH_MEASURE(0.001),#12897,
'DISTANCE_ACCURACY_VALUE',
'Maximum model space distance between geometric entities at asserted c
onnectivities');
#12858=(
GEOMETRIC_REPRESENTATION_CONTEXT(3)
GLOBAL_UNCERTAINTY_ASSIGNED_CONTEXT((#12815))
GLOBAL_UNIT_ASSIGNED_CONTEXT((#12897,#12899,#12900))
REPRESENTATION_CONTEXT('','3D')
);
#12896=(
GEOMETRIC_REPRESENTATION_CONTEXT(3)
GLOBAL_UNCERTAINTY_ASSIGNED_CONTEXT((#12853))
GLOBAL_UNIT_ASSIGNED_CONTEXT((#12897,#12899,#12900))
REPRESENTATION_CONTEXT('','3D')
);
#12897=(
LENGTH_UNIT()
NAMED_UNIT(*)
SI_UNIT(.CENTI.,.METRE.)
);
#12899=(
NAMED_UNIT(*)
PLANE_ANGLE_UNIT()
SI_UNIT($,.RADIAN.)
);
#12900=(
NAMED_UNIT(*)
SI_UNIT($,.STERADIAN.)
SOLID_ANGLE_UNIT()
);
#12905=SHAPE_DEFINITION_REPRESENTATION(#12947,#13058);
#12947=PRODUCT_DEFINITION_SHAPE('',$,#13101);
#13058=SHAPE_REPRESENTATION('',(#6661),#12858);
#13096=PRODUCT_DEFINITION_CONTEXT('part definition',#13224,'design');
#13101=PRODUCT_DEFINITION('Foot (1)','Foot (1)',#13143,#13096);
#13143=PRODUCT_DEFINITION_FORMATION('',$,#13230);
#13224=APPLICATION_CONTEXT(
'Core Data for Automotive Mechanical Design Process');
#13225=PRODUCT_CONTEXT('part definition',#13224,'mechanical');
#13230=PRODUCT('Foot (1)','Foot (1)','Foot (1)',(#13225));
#13338=COLOUR_RGB('Off White',0.89,0.88,0.83);
#13339=FILL_AREA_STYLE_COLOUR('',#13338);
#13340=FILL_AREA_STYLE('',(#13339));
#13341=SURFACE_STYLE_FILL_AREA(#13340);
#13342=SURFACE_SIDE_STYLE('',(#13341));
#13343=SURFACE_STYLE_USAGE(.BOTH.,#13342);
#13344=PRESENTATION_STYLE_ASSIGNMENT((#13343));
ENDSEC;
END-ISO-10303-21;
